ISO-10303-21;
HEADER;
/* Generated by software containing ST-Developer
 * from STEP Tools, Inc. (www.steptools.com) 
 */

FILE_DESCRIPTION(
/* description */ ('Bin tilter linkage'),
/* implementation_level */ '2;1');

FILE_NAME(
/* name */ 'M4 short cap screw (20).step',
/* time_stamp */ '2026-10-28T03:26:24-07:00',
/* author */ (''),
/* organization */ (''),
/* preprocessor_version */ 'ST-DEVELOPER v20.2',
/* originating_system */ 'Autodesk Translation Framework v15.17.0.0',
/* authorisation */ '');

FILE_SCHEMA (('AUTOMOTIVE_DESIGN { 1 0 10303 214 3 1 1 }'));
ENDSEC;

DATA;
#10=MECHANICAL_DESIGN_GEOMETRIC_PRESENTATION_REPRESENTATION('',(#920),#23728);
#708=SHAPE_REPRESENTATION_RELATIONSHIP('SRR','None',#24174,#814);
#814=ADVANCED_BREP_SHAPE_REPRESENTATION('',(#1033),#23674);
#920=STYLED_ITEM('',(#24772),#1033);
#1033=MANIFOLD_SOLID_BREP('Body1',#12451);
#1354=FACE_BOUND('',#3364,.T.);
#1697=PLANE('',#14612);
#1698=PLANE('',#14617);
#1699=PLANE('',#14620);
#2319=FACE_OUTER_BOUND('',#3363,.T.);
#2320=FACE_OUTER_BOUND('',#3365,.T.);
#2321=FACE_OUTER_BOUND('',#3366,.T.);
#2322=FACE_OUTER_BOUND('',#3367,.T.);
#2323=FACE_OUTER_BOUND('',#3368,.T.);
#3363=EDGE_LOOP('',(#9997));
#3364=EDGE_LOOP('',(#9998));
#3365=EDGE_LOOP('',(#9999,#10000,#10001,#10002));
#3366=EDGE_LOOP('',(#10003));
#3367=EDGE_LOOP('',(#10004,#10005,#10006,#10007));
#3368=EDGE_LOOP('',(#10008));
#4217=LINE('',#21597,#4892);
#4218=LINE('',#21601,#4893);
#4892=VECTOR('',#17724,0.350000000000001);
#4893=VECTOR('',#17729,0.199999999999999);
#5643=CIRCLE('',#14613,0.350000000000001);
#5644=CIRCLE('',#14614,0.199999999999999);
#5645=CIRCLE('',#14616,0.350000000000001);
#5646=CIRCLE('',#14619,0.199999999999999);
#6497=VERTEX_POINT('',#21590);
#6498=VERTEX_POINT('',#21592);
#6499=VERTEX_POINT('',#21595);
#6500=VERTEX_POINT('',#21600);
#7738=EDGE_CURVE('',#6497,#6497,#5643,.T.);
#7739=EDGE_CURVE('',#6498,#6498,#5644,.T.);
#7740=EDGE_CURVE('',#6499,#6499,#5645,.T.);
#7741=EDGE_CURVE('',#6499,#6497,#4217,.T.);
#7742=EDGE_CURVE('',#6498,#6500,#4218,.T.);
#7743=EDGE_CURVE('',#6500,#6500,#5646,.T.);
#9997=ORIENTED_EDGE('',*,*,#7738,.F.);
#9998=ORIENTED_EDGE('',*,*,#7739,.T.);
#9999=ORIENTED_EDGE('',*,*,#7740,.F.);
#10000=ORIENTED_EDGE('',*,*,#7741,.T.);
#10001=ORIENTED_EDGE('',*,*,#7738,.T.);
#10002=ORIENTED_EDGE('',*,*,#7741,.F.);
#10003=ORIENTED_EDGE('',*,*,#7740,.T.);
#10004=ORIENTED_EDGE('',*,*,#7739,.F.);
#10005=ORIENTED_EDGE('',*,*,#7742,.T.);
#10006=ORIENTED_EDGE('',*,*,#7743,.T.);
#10007=ORIENTED_EDGE('',*,*,#7742,.F.);
#10008=ORIENTED_EDGE('',*,*,#7743,.F.);
#11487=CYLINDRICAL_SURFACE('',#14615,0.350000000000001);
#11488=CYLINDRICAL_SURFACE('',#14618,0.199999999999999);
#12044=ADVANCED_FACE('',(#2319,#1354),#1697,.F.);
#12045=ADVANCED_FACE('',(#2320),#11487,.T.);
#12046=ADVANCED_FACE('',(#2321),#1698,.T.);
#12047=ADVANCED_FACE('',(#2322),#11488,.T.);
#12048=ADVANCED_FACE('',(#2323),#1699,.F.);
#12451=CLOSED_SHELL('',(#12044,#12045,#12046,#12047,#12048));
#14611=AXIS2_PLACEMENT_3D('',#21588,#17712,#17713);
#14612=AXIS2_PLACEMENT_3D('',#21589,#17714,#17715);
#14613=AXIS2_PLACEMENT_3D('',#21591,#17716,#17717);
#14614=AXIS2_PLACEMENT_3D('',#21593,#17718,#17719);
#14615=AXIS2_PLACEMENT_3D('',#21594,#17720,#17721);
#14616=AXIS2_PLACEMENT_3D('',#21596,#17722,#17723);
#14617=AXIS2_PLACEMENT_3D('',#21598,#17725,#17726);
#14618=AXIS2_PLACEMENT_3D('',#21599,#17727,#17728);
#14619=AXIS2_PLACEMENT_3D('',#21602,#17730,#17731);
#14620=AXIS2_PLACEMENT_3D('',#21603,#17732,#17733);
#17712=DIRECTION('axis',(0.,0.,1.));
#17713=DIRECTION('refdir',(1.,0.,0.));
#17714=DIRECTION('center_axis',(0.,1.,0.));
#17715=DIRECTION('ref_axis',(1.,0.,0.));
#17716=DIRECTION('center_axis',(0.,1.,0.));
#17717=DIRECTION('ref_axis',(1.,0.,0.));
#17718=DIRECTION('center_axis',(0.,1.,0.));
#17719=DIRECTION('ref_axis',(1.,0.,0.));
#17720=DIRECTION('center_axis',(0.,1.,0.));
#17721=DIRECTION('ref_axis',(1.,0.,0.));
#17722=DIRECTION('center_axis',(0.,1.,0.));
#17723=DIRECTION('ref_axis',(1.,0.,0.));
#17724=DIRECTION('',(0.,-1.,0.));
#17725=DIRECTION('center_axis',(0.,1.,0.));
#17726=DIRECTION('ref_axis',(1.,0.,0.));
#17727=DIRECTION('center_axis',(0.,1.,0.));
#17728=DIRECTION('ref_axis',(1.,0.,0.));
#17729=DIRECTION('',(0.,-1.,0.));
#17730=DIRECTION('center_axis',(0.,1.,0.));
#17731=DIRECTION('ref_axis',(1.,0.,0.));
#17732=DIRECTION('center_axis',(0.,1.,0.));
#17733=DIRECTION('ref_axis',(1.,0.,0.));
#21588=CARTESIAN_POINT('',(0.,0.,0.));
#21589=CARTESIAN_POINT('Origin',(19.3081475451951,0.8,16.3081475451951));
#21590=CARTESIAN_POINT('',(18.9581475451951,0.8,16.3081475451951));
#21591=CARTESIAN_POINT('Origin',(19.3081475451951,0.8,16.3081475451951));
#21592=CARTESIAN_POINT('',(19.1081475451951,0.8,16.3081475451951));
#21593=CARTESIAN_POINT('Origin',(19.3081475451951,0.8,16.3081475451951));
#21594=CARTESIAN_POINT('Origin',(19.3081475451951,0.8,16.3081475451951));
#21595=CARTESIAN_POINT('',(18.9581475451951,1.2,16.3081475451951));
#21596=CARTESIAN_POINT('Origin',(19.3081475451951,1.2,16.3081475451951));
#21597=CARTESIAN_POINT('',(18.9581475451951,0.8,16.3081475451951));
#21598=CARTESIAN_POINT('Origin',(19.3081475451951,1.2,16.3081475451951));
#21599=CARTESIAN_POINT('Origin',(19.3081475451951,0.1,16.3081475451951));
#21600=CARTESIAN_POINT('',(19.1081475451951,0.1,16.3081475451951));
#21601=CARTESIAN_POINT('',(19.1081475451951,0.1,16.3081475451951));
#21602=CARTESIAN_POINT('Origin',(19.3081475451951,0.1,16.3081475451951));
#21603=CARTESIAN_POINT('Origin',(19.3081475451951,0.1,16.3081475451951));
#23557=UNCERTAINTY_MEASURE_WITH_UNIT(LENGTH_MEASURE(0.001),#23729,
'DISTANCE_ACCURACY_VALUE',
'Maximum model space distance between geometric entities at asserted c
onnectivities');
#23611=UNCERTAINTY_MEASURE_WITH_UNIT(LENGTH_MEASURE(0.001),#23729,
'DISTANCE_ACCURACY_VALUE',
'Maximum model space distance between geometric entities at asserted c
onnectivities');
#23674=(
GEOMETRIC_REPRESENTATION_CONTEXT(3)
GLOBAL_UNCERTAINTY_ASSIGNED_CONTEXT((#23557))
GLOBAL_UNIT_ASSIGNED_CONTEXT((#23729,#23731,#23732))
REPRESENTATION_CONTEXT('','3D')
);
#23728=(
GEOMETRIC_REPRESENTATION_CONTEXT(3)
GLOBAL_UNCERTAINTY_ASSIGNED_CONTEXT((#23611))
GLOBAL_UNIT_ASSIGNED_CONTEXT((#23729,#23731,#23732))
REPRESENTATION_CONTEXT('','3D')
);
#23729=(
LENGTH_UNIT()
NAMED_UNIT(*)
SI_UNIT(.CENTI.,.METRE.)
);
#23731=(
NAMED_UNIT(*)
PLANE_ANGLE_UNIT()
SI_UNIT($,.RADIAN.)
);
#23732=(
NAMED_UNIT(*)
SI_UNIT($,.STERADIAN.)
SOLID_ANGLE_UNIT()
);
#23795=SHAPE_DEFINITION_REPRESENTATION(#23911,#24174);
#23911=PRODUCT_DEFINITION_SHAPE('',$,#24291);
#24174=SHAPE_REPRESENTATION('',(#14611),#23674);
#24228=PRODUCT_DEFINITION_CONTEXT('part definition',#24578,'design');
#24291=PRODUCT_DEFINITION('M4 short cap screw (20)',
'M4 short cap screw (20)',#24407,#24228);
#24407=PRODUCT_DEFINITION_FORMATION('',$,#24642);
#24578=APPLICATION_CONTEXT(
'Core Data for Automotive Mechanical Design Process');
#24579=PRODUCT_CONTEXT('part definition',#24578,'mechanical');
#24642=PRODUCT('M4 short cap screw (20)','M4 short cap screw (20)',
'M4 short cap screw (20)',(#24579));
#24766=COLOUR_RGB('Black',0.12,0.14,0.17);
#24767=FILL_AREA_STYLE_COLOUR('',#24766);
#24768=FILL_AREA_STYLE('',(#24767));
#24769=SURFACE_STYLE_FILL_AREA(#24768);
#24770=SURFACE_SIDE_STYLE('',(#24769));
#24771=SURFACE_STYLE_USAGE(.BOTH.,#24770);
#24772=PRESENTATION_STYLE_ASSIGNMENT((#24771));
ENDSEC;
END-ISO-10303-21;
